ISO-10303-21;
HEADER;
FILE_DESCRIPTION (('STEP AP203'),
    '1' );
FILE_NAME ('Pin.step',
    '2026-10-31T14:11:27',
    ( '' ),
    ( '' ),
    'SwSTEP 2.0',
    'SolidWorks 2024',
    '' );
FILE_SCHEMA (( 'AUTOMOTIVE_DESIGN' ));
ENDSEC;

DATA;
#24=DIRECTION ( 'NONE',  ( -0.9999862922474493931, -0.005235963827107929618, 0.000000000000000000 ) ) ;
#31=CARTESIAN_POINT ( 'NONE',  ( -62.94230935805129690, 13.36384453327990052, -5.515482965309170069E-15 ) ) ;
#59=ORIENTED_EDGE ( 'NONE', *, *, #12413, .F. ) ;
#109=CARTESIAN_POINT ( 'NONE',  ( -64.07944010525029910, -25.33596492959100388, 4.999999999999991118 ) ) ;
#119=ORIENTED_EDGE ( 'NONE', *, *, #12198, .T. ) ;
#129=ADVANCED_FACE ( 'NONE', ( #12049 ), #13926, .T. ) ;
#132=LINE ( 'NONE', #14633, #21183 ) ;
#168=EDGE_LOOP ( 'NONE', ( #10288, #18561, #2673, #1154, #10285 ) ) ;
#254=ORIENTED_EDGE ( 'NONE', *, *, #5018, .F. ) ;
#356=VECTOR ( 'NONE', #17095, 1000.000000000000000 ) ;
#415=DIRECTION ( 'NONE',  ( 1.000000000000000000, 0.000000000000000000, 0.000000000000000000 ) ) ;
#443=DIRECTION ( 'NONE',  ( 6.009176021521548497E-19, -0.9999588795606766389, -0.009068582455715215943 ) ) ;
#453=DIRECTION ( 'NONE',  ( -0.005235963827108352890, 0.9999862922474493931, 5.936218956694023463E-19 ) ) ;
#461=CARTESIAN_POINT ( 'NONE',  ( -62.75934763415060047, -21.57895147295310068, -5.536226058455569256E-15 ) ) ;
#521=CIRCLE ( 'NONE', #4340, 4.999999999999995559 ) ;
#573=EDGE_LOOP ( 'NONE', ( #11561, #21123, #806, #4232, #14126, #5854, #13368 ) ) ;
#614=AXIS2_PLACEMENT_3D ( 'NONE', #10276, #10510, #19288 ) ;
#627=CARTESIAN_POINT ( 'NONE',  ( -62.73971250800079957, -25.32895006819559924, -5.000000000000000000 ) ) ;
#631=CARTESIAN_POINT ( 'NONE',  ( -67.10797875267205370, -21.85177448797741917, -6.069095851239679835E-15 ) ) ;
#662=FACE_OUTER_BOUND ( 'NONE', #16612, .T. ) ;
#685=ADVANCED_FACE ( 'NONE', ( #2454 ), #9804, .T. ) ;
#713=CARTESIAN_POINT ( 'NONE',  ( -59.07950864401301772, -25.30978511045550050, 3.660254037844370423 ) ) ;
#806=ORIENTED_EDGE ( 'NONE', *, *, #4181, .T. ) ;
#808=CARTESIAN_POINT ( 'NONE',  ( -62.74088165156670271, -25.10566213532069924, -5.538319619822460249E-15 ) ) ;
#877=PLANE ( 'NONE',  #20182 ) ;
#969=ORIENTED_EDGE ( 'NONE', *, *, #9231, .F. ) ;
#1012=ADVANCED_FACE ( 'NONE', ( #7078 ), #21648, .T. ) ;
#1042=DIRECTION ( 'NONE',  ( 0.9999862922474493931, 0.005235963827108368503, 0.000000000000000000 ) ) ;
#1150=VECTOR ( 'NONE', #12142, 1000.000000000000000 ) ;
#1154=ORIENTED_EDGE ( 'NONE', *, *, #5018, .T. ) ;
#1167=CARTESIAN_POINT ( 'NONE',  ( -68.51547434528259828, -24.91260405369630249, -2.885287058652779450E-14 ) ) ;
#1212=AXIS2_PLACEMENT_3D ( 'NONE', #4249, #19109, #17316 ) ;
#1312=LINE ( 'NONE', #22806, #7881 ) ;
#1326=FACE_OUTER_BOUND ( 'NONE', #573, .T. ) ;
#1336=DIRECTION ( 'NONE',  ( 0.9999862922474493931, 0.005235963827108368503, 0.000000000000000000 ) ) ;
#1366=PLANE ( 'NONE',  #15411 ) ;
#1377=ORIENTED_EDGE ( 'NONE', *, *, #9871, .T. ) ;
#1453=CARTESIAN_POINT ( 'NONE',  ( -62.73971250800079957, -25.32895006819559924, -5.538452170245418869E-15 ) ) ;
#1486=ORIENTED_EDGE ( 'NONE', *, *, #19639, .F. ) ;
#1496=CARTESIAN_POINT ( 'NONE',  ( -65.64475015647069256, -21.84411297095480009, 5.000000000000000000 ) ) ;
#1497=AXIS2_PLACEMENT_3D ( 'NONE', #461, #7728, #13192 ) ;
#1524=( BOUNDED_CURVE ( )  B_SPLINE_CURVE ( 2, ( #13608, #8157, #22733 ),
 .UNSPECIFIED., .F., .F. ) 
 B_SPLINE_CURVE_WITH_KNOTS ( ( 3, 3 ),
 ( 0.2928548593876180162, 0.5857097187752360323 ),
 .UNSPECIFIED. ) 
 CURVE ( )  GEOMETRIC_REPRESENTATION_ITEM ( )  RATIONAL_B_SPLINE_CURVE ( ( 1.000000000000000000, 1.037954849302029858, 1.000000000000000000 ) ) 
 REPRESENTATION_ITEM ( '' )  );
#1539=ADVANCED_FACE ( 'NONE', ( #10739 ), #3797, .T. ) ;
#1567=EDGE_CURVE ( 'NONE', #22209, #6518, #19393, .T. ) ;
#1702=CARTESIAN_POINT ( 'NONE',  ( -62.73971250800079957, -25.32895006819559924, -5.538452170245418869E-15 ) ) ;
#1714=DIRECTION ( 'NONE',  ( -4.033639808943980242E-37, 5.936300330036069670E-19, -1.000000000000000000 ) ) ;
#1736=CARTESIAN_POINT ( 'NONE',  ( -68.51547434528259828, -24.91260405369630249, -2.885287058652779450E-14 ) ) ;
#1741=ORIENTED_EDGE ( 'NONE', *, *, #10031, .F. ) ;
#1782=VERTEX_POINT ( 'NONE', #11327 ) ;
#1852=EDGE_CURVE ( 'NONE', #15219, #8168, #14582, .T. ) ;
#1915=DIRECTION ( 'NONE',  ( -0.005235963827108352890, 0.9999862922474493931, 5.936218956694023463E-19 ) ) ;
#1917=CLOSED_SHELL ( 'NONE', ( #2769, #13548, #5082, #6507, #15599, #11687, #1539, #685, #12602, #19975, #129, #4126, #23045, #6384, #3776, #21888, #21015, #21119, #12737, #7471, #15663, #22262, #1012 ) ) ;
#1927=CARTESIAN_POINT ( 'NONE',  ( -62.94391562085439773, 13.67061532808409829, -5.515300856952130332E-15 ) ) ;
#2014=AXIS2_PLACEMENT_3D ( 'NONE', #8864, #12766, #1714 ) ;
#2022=MANIFOLD_SOLID_BREP ( 'Boss-Extrude1', #1917 ) ;
#2023=CARTESIAN_POINT ( 'NONE',  ( -65.62876257020761273, -24.89748912807110059, 5.000000000000000000 ) ) ;
#2031=VERTEX_POINT ( 'NONE', #3320 ) ;
#2037=DIRECTION ( 'NONE',  ( 1.000000000000000000, -1.922967408714619726E-16, 0.000000000000000000 ) ) ;
#2085=EDGE_LOOP ( 'NONE', ( #16858, #59, #11665 ) ) ;
#2119=DIRECTION ( 'NONE',  ( 0.8660135325225010172, 0.004534477687572223414, -0.5000000000000000000 ) ) ;
#2249=FACE_OUTER_BOUND ( 'NONE', #18547, .T. ) ;
#2362=DIRECTION ( 'NONE',  ( 0.005235963827108352890, -0.9999862922474493931, -5.936218956694023463E-19 ) ) ;
#2387=EDGE_CURVE ( 'NONE', #9101, #2031, #8977, .T. ) ;
#2390=AXIS2_PLACEMENT_3D ( 'NONE', #19292, #6713, #21419 ) ;
#2454=FACE_OUTER_BOUND ( 'NONE', #19325, .T. ) ;
#2503=DIRECTION ( 'NONE',  ( -0.7033367706102514605, -0.7108567978907863738, -4.197882762799809725E-19 ) ) ;
#2506=CARTESIAN_POINT ( 'NONE',  ( -56.96862724498259922, -24.85214435119530307, -5.538187069399500051E-15 ) ) ;
#2569=CARTESIAN_POINT ( 'NONE',  ( 0.000000000000000000, 0.000000000000000000, 0.000000000000000000 ) ) ;
#2570=CARTESIAN_POINT ( 'NONE',  ( -62.82872441665805496, -8.329083101359751495, -5.528360538656856695E-15 ) ) ;
#2574=ORIENTED_EDGE ( 'NONE', *, *, #11403, .F. ) ;
#2575=DIRECTION ( 'NONE',  ( 0.005235963827108302583, -0.9999862922474493931, -5.936218956694023463E-19 ) ) ;
#2579=CARTESIAN_POINT ( 'NONE',  ( -67.06978017061331343, -25.35162245663349978, -2.500000000000000000 ) ) ;
#2673=ORIENTED_EDGE ( 'NONE', *, *, #8047, .F. ) ;
#2754=CIRCLE ( 'NONE', #18706, 4.349999999999976552 ) ;
#2769=ADVANCED_FACE ( 'NONE', ( #22710 ), #19178, .T. ) ;
#2886=DIRECTION ( 'NONE',  ( -0.005235963827108231460, 0.9999862922474493931, 2.671135040551772162E-18 ) ) ;
#2893=DIRECTION ( 'NONE',  ( -0.005235963827108362431, 0.9999862922474493931, 5.936218956694023463E-19 ) ) ;
#2932=CARTESIAN_POINT ( 'NONE',  ( -57.73978104676356793, -25.30277024906009586, -1.339745962155629577 ) ) ;
#2945=EDGE_CURVE ( 'NONE', #18682, #9640, #14639, .T. ) ;
#2958=AXIS2_PLACEMENT_3D ( 'NONE', #808, #9641, #16855 ) ;
#2988=ORIENTED_EDGE ( 'NONE', *, *, #15770, .F. ) ;
#3053=LINE ( 'NONE', #19791, #14108 ) ;
#3105=CONICAL_SURFACE ( 'NONE', #12614, 5.386751345948120218, 1.047197551196598297 ) ;
#3107=EDGE_CURVE ( 'NONE', #9845, #8168, #8188, .T. ) ;
#3111=CARTESIAN_POINT ( 'NONE',  ( -66.39991637198865249, -25.34811502593582944, 3.660254037844372199 ) ) ;
#3165=DIRECTION ( 'NONE',  ( 0.005235963827108352890, -0.9999862922474493931, -2.671135040551771006E-18 ) ) ;
#3261=DIRECTION ( 'NONE',  ( -0.9999862922474493931, -0.005235963827108420544, 0.000000000000000000 ) ) ;
#3320=CARTESIAN_POINT ( 'NONE',  ( -67.17866478793438034, -8.351859544007679048, -6.061081896285953642E-15 ) ) ;
#3329=CIRCLE ( 'NONE', #18522, 3.000000000000001332 ) ;
#3358=EDGE_CURVE ( 'NONE', #23387, #17399, #14937, .T. ) ;
#3362=DIRECTION ( 'NONE',  ( 0.8660135325225010172, 0.004534477687572227751, 0.5000000000000000000 ) ) ;
#3458=ORIENTED_EDGE ( 'NONE', *, *, #11403, .T. ) ;
#3528=EDGE_CURVE ( 'NONE', #12983, #7920, #13621, .T. ) ;
#3593=DIRECTION ( 'NONE',  ( 0.9999862922474493931, 0.005235963827108502076, 0.000000000000000000 ) ) ;
#3606=PRODUCT ( 'Pin', 'Pin', '', ( #17260 ) ) ;
#3633=CARTESIAN_POINT ( 'NONE',  ( -58.40809801011923241, -21.80622160268157828, -5.536374493610581309E-15 ) ) ;
#3653=ORIENTED_EDGE ( 'NONE', *, *, #11974, .T. ) ;
#3699=ORIENTED_EDGE ( 'NONE', *, *, #3528, .T. ) ;
#3706=DIRECTION ( 'NONE',  ( -0.005235963827108352890, 0.9999862922474493931, 5.936218956694023463E-19 ) ) ;
#3730=CARTESIAN_POINT ( 'NONE',  ( -65.62876257020761273, -24.89748912807110059, -5.000000000000000000 ) ) ;
#3732=DIRECTION ( 'NONE',  ( -0.005235963827108352890, 0.9999862922474493931, 5.936218956694023463E-19 ) ) ;
#3747=ORIENTED_EDGE ( 'NONE', *, *, #18867, .T. ) ;
#3755=VECTOR ( 'NONE', #18817, 1000.000000000000000 ) ;
#3760=FACE_OUTER_BOUND ( 'NONE', #5998, .T. ) ;
#3776=ADVANCED_FACE ( 'NONE', ( #5411 ), #22016, .T. ) ;
#3797=CONICAL_SURFACE ( 'NONE', #4571, 5.386751345948120218, 1.047197551196598297 ) ;
#3868=DIRECTION ( 'NONE',  ( 0.9999862922474493931, 0.005235963827108502076, 0.000000000000000000 ) ) ;
#3887=DIRECTION ( 'NONE',  ( -0.005235963827108231460, 0.9999862922474493931, 5.936218956694025389E-19 ) ) ;
#3962=DIRECTION ( 'NONE',  ( 0.9999862922474493931, 0.005235963827108368503, 0.000000000000000000 ) ) ;
#3968=( BOUNDED_CURVE ( )  B_SPLINE_CURVE ( 2, ( #627, #22487, #20353 ),
 .UNSPECIFIED., .F., .F. ) 
 B_SPLINE_CURVE_WITH_KNOTS ( ( 3, 3 ),
 ( 0.2928548593876180162, 0.5857097187752360323 ),
 .UNSPECIFIED. ) 
 CURVE ( )  GEOMETRIC_REPRESENTATION_ITEM ( )  RATIONAL_B_SPLINE_CURVE ( ( 1.000000000000000000, 1.037954849302059834, 1.000000000000000000 ) ) 
 REPRESENTATION_ITEM ( '' )  );
#4003=DIRECTION ( 'NONE',  ( -0.9999862922474492821, -0.005235963827108258348, 0.000000000000000000 ) ) ;
#4023=EDGE_CURVE ( 'NONE', #6518, #18157, #16762, .T. ) ;
#4065=ORIENTED_EDGE ( 'NONE', *, *, #10833, .T. ) ;
#4082=CONICAL_SURFACE ( 'NONE', #14321, 2.693275000000006081, 0.7853166638051269910 ) ;
#4126=ADVANCED_FACE ( 'NONE', ( #13709 ), #10411, .T. ) ;
#4154=VECTOR ( 'NONE', #1915, 1000.000000000000000 ) ;
#4161=ORIENTED_EDGE ( 'NONE', *, *, #11974, .F. ) ;
#4181=EDGE_CURVE ( 'NONE', #16628, #15219, #17172, .T. ) ;
#4220=EDGE_LOOP ( 'NONE', ( #4161, #17253 ) ) ;
#4232=ORIENTED_EDGE ( 'NONE', *, *, #15770, .T. ) ;
#4249=CARTESIAN_POINT ( 'NONE',  ( -62.74088165156670271, -25.10566213532069924, -5.538319619822460249E-15 ) ) ;
#4272=ORIENTED_EDGE ( 'NONE', *, *, #15333, .T. ) ;
#4321=ORIENTED_EDGE ( 'NONE', *, *, #10833, .F. ) ;
#4340=AXIS2_PLACEMENT_3D ( 'NONE', #19000, #15075, #1042 ) ;
#4371=CARTESIAN_POINT ( 'NONE',  ( -67.06978017061331343, -25.35162245663349978, 2.500000000000000000 ) ) ;
#4461=CIRCLE ( 'NONE', #17738, 4.999999999999995559 ) ;
#4558=CARTESIAN_POINT ( 'NONE',  ( -62.74088165156670271, -25.10566213532069924, -5.538319619822460249E-15 ) ) ;
#4571=AXIS2_PLACEMENT_3D ( 'NONE', #21164, #13929, #3593 ) ;
#4645=CONICAL_SURFACE ( 'NONE', #17920, 5.386751345948120218, 1.047197551196598297 ) ;
#4665=ORIENTED_EDGE ( 'NONE', *, *, #17709, .T. ) ;
#4673=CARTESIAN_POINT ( 'NONE',  ( -62.73971250800079957, -25.32895006819559924, -5.260896414089139989E-15 ) ) ;
#4825=CIRCLE ( 'NONE', #18106, 4.349999999999976552 ) ;
#4858=CARTESIAN_POINT ( 'NONE',  ( -59.87132660632070014, -21.81388311970430038, 5.000000000000000000 ) ) ;
#4885=LINE ( 'NONE', #20909, #1150 ) ;
#4964=ORIENTED_EDGE ( 'NONE', *, *, #11294, .T. ) ;
#5018=EDGE_CURVE ( 'NONE', #7920, #5108, #14725, .T. ) ;
#5038=CARTESIAN_POINT ( 'NONE',  ( -62.82872441665799101, -8.329083101359751495, -5.528360538656857483E-15 ) ) ;
#5070=AXIS2_PLACEMENT_3D ( 'NONE', #14163, #22821, #19168 ) ;
#5073=DIRECTION ( 'NONE',  ( -0.5000051404512463327, 0.000000000000000000, 0.8660224359231865066 ) ) ;
#5082=ADVANCED_FACE ( 'NONE', ( #2249 ), #16732, .T. ) ;
#5108=VERTEX_POINT ( 'NONE', #1167 ) ;
#5247=CARTESIAN_POINT ( 'NONE',  ( -60.24907127679855279, 13.37794642375635590, -5.845314026106529258E-15 ) ) ;
#5258=ORIENTED_EDGE ( 'NONE', *, *, #18536, .T. ) ;
#5356=EDGE_LOOP ( 'NONE', ( #12461, #22910, #18015, #1741 ) ) ;
#5407=CARTESIAN_POINT ( 'NONE',  ( -57.35420414587308358, -25.07745730012768703, -5.538319619822460249E-15 ) ) ;
#5408=ORIENTED_EDGE ( 'NONE', *, *, #15063, .F. ) ;
#5411=FACE_OUTER_BOUND ( 'NONE', #14757, .T. ) ;
#5461=LINE ( 'NONE', #14602, #19084 ) ;
#5572=CARTESIAN_POINT ( 'NONE',  ( -62.75803838139569280, -21.82899804532949872, -5.536374493610579731E-15 ) ) ;
#5601=ORIENTED_EDGE ( 'NONE', *, *, #13690, .F. ) ;
#5617=CONICAL_SURFACE ( 'NONE', #2958, 5.386751345948120218, 1.047197551196598297 ) ;
#5619=CARTESIAN_POINT ( 'NONE',  ( -66.39991637198862406, -25.34811502593583654, -3.660254037844378860 ) ) ;
#5626=EDGE_CURVE ( 'NONE', #8174, #10214, #14800, .T. ) ;
#5692=EDGE_LOOP ( 'NONE', ( #12860, #2988, #22621 ) ) ;
#5795=APPLICATION_CONTEXT ( 'configuration controlled 3d designs of mechanical parts and assemblies' ) ;
#5836=CARTESIAN_POINT ( 'NONE',  ( -59.94074421850589829, 13.07278162995702431, -5.883059113410419196E-15 ) ) ;
#5854=ORIENTED_EDGE ( 'NONE', *, *, #13690, .T. ) ;
#5884=CARTESIAN_POINT ( 'NONE',  ( -62.94391562085439773, 13.67061532808409829, -5.515300856952130332E-15 ) ) ;
#5924=EDGE_CURVE ( 'NONE', #1782, #22209, #18179, .T. ) ;
#5998=EDGE_LOOP ( 'NONE', ( #11906, #20666 ) ) ;
#5999=DIRECTION ( 'NONE',  ( -0.9999862922474493931, -0.005235963827107929618, 0.000000000000000000 ) ) ;
#6026=CARTESIAN_POINT ( 'NONE',  ( -68.51547434528259828, -24.91260405369630249, -2.885287058652779450E-14 ) ) ;
#6057=EDGE_CURVE ( 'NONE', #14376, #20293, #11349, .T. ) ;
#6096=CIRCLE ( 'NONE', #19369, 2.999999999999994227 ) ;
#6162=ORIENTED_EDGE ( 'NONE', *, *, #18536, .F. ) ;
#6300=FACE_OUTER_BOUND ( 'NONE', #21298, .T. ) ;
#6384=ADVANCED_FACE ( 'NONE', ( #7270, #17967 ), #12623, .T. ) ;
#6395=ORIENTED_EDGE ( 'NONE', *, *, #1567, .T. ) ;
#6399=CARTESIAN_POINT ( 'NONE',  ( -56.98461483124570037, -21.79876819407909849, -1.072991366992009803E-14 ) ) ;
#6507=ADVANCED_FACE ( 'NONE', ( #6300 ), #4645, .T. ) ;
#6518=VERTEX_POINT ( 'NONE', #5836 ) ;
#6584=AXIS2_PLACEMENT_3D ( 'NONE', #1702, #12530, #3962 ) ;
#6612=EDGE_CURVE ( 'NONE', #1782, #18157, #13539, .T. ) ;
#6713=DIRECTION ( 'NONE',  ( 0.005235963827108352890, -0.9999862922474493931, -2.671135040551771006E-18 ) ) ;
#6757=CIRCLE ( 'NONE', #20017, 4.999999999999995559 ) ;
#6826=UNCERTAINTY_MEASURE_WITH_UNIT (LENGTH_MEASURE( 1.000000000000000082E-05 ), #13320, 'distance_accuracy_value', 'NONE');
#6857=CARTESIAN_POINT ( 'NONE',  ( -58.40964484538829993, -25.30627767975780174, -2.500000000000000000 ) ) ;
#6864=EDGE_LOOP ( 'NONE', ( #4321, #15777 ) ) ;
#6929=PLANE ( 'NONE',  #5070 ) ;
#6951=ORIENTED_EDGE ( 'NONE', *, *, #13841, .F. ) ;
#7003=CARTESIAN_POINT ( 'NONE',  ( -67.73964396923798859, -25.35512988733120565, -1.339745962155620029 ) ) ;
#7035=AXIS2_PLACEMENT_3D ( 'NONE', #11405, #2119, #443 ) ;
#7078=FACE_OUTER_BOUND ( 'NONE', #5356, .T. ) ;
#7088=CARTESIAN_POINT ( 'NONE',  ( -67.10928800542700401, -21.60172791560102112, -6.068947416084667781E-15 ) ) ;
#7114=AXIS2_PLACEMENT_3D ( 'NONE', #5572, #453, #18418 ) ;
#7170=LINE ( 'NONE', #12636, #4154 ) ;
#7203=DIRECTION ( 'NONE',  ( -1.000000000000000000, 0.000000000000000000, 7.691776389375310104E-16 ) ) ;
#7270=FACE_OUTER_BOUND ( 'NONE', #14855, .T. ) ;
#7304=DIRECTION ( 'NONE',  ( 0.005235963827108302583, -0.9999862922474493931, -5.936218956694023463E-19 ) ) ;
#7329=EDGE_LOOP ( 'NONE', ( #18779, #6951, #6162 ) ) ;
#7391=ORIENTED_EDGE ( 'NONE', *, *, #4023, .F. ) ;
#7471=ADVANCED_FACE ( 'NONE', ( #18223, #10890 ), #12423, .F. ) ;
#7488=CARTESIAN_POINT ( 'NONE',  ( -59.85533902005759899, -24.86725927682059734, -5.000000000000000000 ) ) ;
#7518=CARTESIAN_POINT ( 'NONE',  ( -59.85533902005759899, -24.86725927682059734, 5.000000000000000000 ) ) ;
#7549=CARTESIAN_POINT ( 'NONE',  ( -59.87132660632070014, -21.81388311970430038, -5.000000000000000000 ) ) ;
#7571=DIRECTION ( 'NONE',  ( 1.133739489558799860E-16, 7.703614176864520825E-35, 1.000000000000000000 ) ) ;
#7597=FACE_OUTER_BOUND ( 'NONE', #2085, .T. ) ;
#7608=CARTESIAN_POINT ( 'NONE',  ( -62.74088165156670271, -25.10566213532069924, -5.538319619822460249E-15 ) ) ;
#7696=EDGE_CURVE ( 'NONE', #23387, #16843, #21594, .T. ) ;
#7713=CARTESIAN_POINT ( 'NONE',  ( -68.53146193154570653, -21.85922789657999843, -2.680796741387739937E-15 ) ) ;
#7726=ORIENTED_EDGE ( 'NONE', *, *, #17709, .F. ) ;
#7728=DIRECTION ( 'NONE',  ( -0.005235963827108352890, 0.9999862922474493931, 5.936218956694023463E-19 ) ) ;
#7864=AXIS2_PLACEMENT_3D ( 'NONE', #31, #7304, #3261 ) ;
#7881=VECTOR ( 'NONE', #19372, 1000.000000000000114 ) ;
#7920=VERTEX_POINT ( 'NONE', #7713 ) ;
#7921=DIRECTION ( 'NONE',  ( -0.9999862922474493931, -0.005235963827108420544, 0.000000000000000000 ) ) ;
#7978=SHAPE_REPRESENTATION_RELATIONSHIP ( 'NONE' , 'NONE' ,  #22961, #18729 ) ;
#8045=CIRCLE ( 'NONE', #20933, 4.999999999999995559 ) ;
#8047=EDGE_CURVE ( 'NONE', #7920, #23387, #5461, .T. ) ;
#8067=CARTESIAN_POINT ( 'NONE',  ( -56.96862724498259922, -24.85214435119530307, -5.538187069399500051E-15 ) ) ;
#8095=ORIENTED_EDGE ( 'NONE', *, *, #9589, .T. ) ;
#8109=CARTESIAN_POINT ( 'NONE',  ( -56.98461483124570037, -21.79876819407909849, -1.072991366992009803E-14 ) ) ;
#8112=EDGE_CURVE ( 'NONE', #16843, #15787, #16850, .T. ) ;
#8135=AXIS2_PLACEMENT_3D ( 'NONE', #13476, #11483, #9693 ) ;
#8157=CARTESIAN_POINT ( 'NONE',  ( -61.39998491075132847, -25.32193520680032961, 4.999999999999990230 ) ) ;
#8168=VERTEX_POINT ( 'NONE', #8067 ) ;
#8174=VERTEX_POINT ( 'NONE', #22649 ) ;
#8188=LINE ( 'NONE', #6399, #16947 ) ;
#8198=VECTOR ( 'NONE', #3732, 1000.000000000000000 ) ;
#8245=CONICAL_SURFACE ( 'NONE', #7864, 2.693275000000006081, 0.7853166638051269910 ) ;
#8256=ORIENTED_EDGE ( 'NONE', *, *, #5924, .T. ) ;
#8309=ORIENTED_EDGE ( 'NONE', *, *, #3107, .T. ) ;
#8335=DIRECTION ( 'NONE',  ( 0.005235963827110212514, -0.9999862922474493931, -5.936218956700083401E-19 ) ) ;
#8367=DIRECTION ( 'NONE',  ( 0.000000000000000000, -0.9999588795606766389, 0.009068582455715226351 ) ) ;
#8392=EDGE_LOOP ( 'NONE', ( #3458, #119, #13932, #8778, #9760 ) ) ;
#8393=DIRECTION ( 'NONE',  ( 0.9999862922474493931, 0.005235963827108368503, 0.000000000000000000 ) ) ;
#8408=DIRECTION ( 'NONE',  ( -0.005235963827108352890, 0.9999862922474493931, 5.936218956694023463E-19 ) ) ;
#8420=EDGE_LOOP ( 'NONE', ( #10086, #254, #14976, #1377, #20733 ) ) ;
#8587=CARTESIAN_POINT ( 'NONE',  ( -65.62876257020761273, -24.89748912807110059, 5.000000000000000000 ) ) ;
#8606=EDGE_LOOP ( 'NONE', ( #14122, #11978, #17660, #4065 ) ) ;
#8614=DIRECTION ( 'NONE',  ( -0.005235963827108352890, 0.9999862922474493931, 5.936218956694023463E-19 ) ) ;
#8632=CARTESIAN_POINT ( 'NONE',  ( -65.64475015647069256, -21.84411297095480009, -5.000000000000000000 ) ) ;
#8663=DIRECTION ( 'NONE',  ( 0.005235963827108352890, -0.9999862922474493931, -2.671135040551771006E-18 ) ) ;
#8692=( BOUNDED_CURVE ( )  B_SPLINE_CURVE ( 2, ( #23239, #7003, #1736 ),
 .UNSPECIFIED., .F., .F. ) 
 B_SPLINE_CURVE_WITH_KNOTS ( ( 3, 3 ),
 ( 0.2928548593876180162, 0.5857097187752370315 ),
 .UNSPECIFIED. ) 
 CURVE ( )  GEOMETRIC_REPRESENTATION_ITEM ( )  RATIONAL_B_SPLINE_CURVE ( ( 1.000000000000000000, 1.037954849302019866, 1.000000000000000000 ) ) 
 REPRESENTATION_ITEM ( '' )  );
#8750=VECTOR ( 'NONE', #10390, 1000.000000000000227 ) ;
#8778=ORIENTED_EDGE ( 'NONE', *, *, #7696, .F. ) ;
#8839=( BOUNDED_CURVE ( )  B_SPLINE_CURVE ( 2, ( #7518, #713, #22330 ),
 .UNSPECIFIED., .F., .F. ) 
 B_SPLINE_CURVE_WITH_KNOTS ( ( 3, 3 ),
 ( 0.000000000000000000, 0.2928548593876180162 ),
 .UNSPECIFIED. ) 
 CURVE ( )  GEOMETRIC_REPRESENTATION_ITEM ( )  RATIONAL_B_SPLINE_CURVE ( ( 1.000000000000000000, 1.037954849302029858, 1.000000000000000000 ) ) 
 REPRESENTATION_ITEM ( '' )  );
#8858=AXIS2_PLACEMENT_3D ( 'NONE', #4673, #2886, #10148 ) ;
#8864=CARTESIAN_POINT ( 'NONE',  ( -62.82872441665799101, -8.329083101359751495, -7.727128097349530051E-15 ) ) ;
#8948=CARTESIAN_POINT ( 'NONE',  ( -59.87132660632070014, -21.81388311970430038, -5.000000000000000000 ) ) ;
#8958=VERTEX_POINT ( 'NONE', #3730 ) ;
#8977=LINE ( 'NONE', #7088, #8198 ) ;
#8988=ORIENTED_EDGE ( 'NONE', *, *, #6612, .F. ) ;
#9068=DIRECTION ( 'NONE',  ( 0.005235963827108232327, -0.9999862922474493931, -5.936218956694023463E-19 ) ) ;
#9101=VERTEX_POINT ( 'NONE', #631 ) ;
#9121=CARTESIAN_POINT ( 'NONE',  ( -61.44393618248319910, 13.67846927382480082, -5.515300856952130332E-15 ) ) ;
#9159=DIRECTION ( 'NONE',  ( 5.101515458763170175E-16, 0.000000000000000000, 1.000000000000000000 ) ) ;
#9170=FACE_OUTER_BOUND ( 'NONE', #8606, .T. ) ;
#9205=DIRECTION ( 'NONE',  ( 0.005235963827108352890, -0.9999862922474493931, -2.671135040551771006E-18 ) ) ;
#9231=EDGE_CURVE ( 'NONE', #9101, #18682, #15328, .T. ) ;
#9330=ORIENTED_EDGE ( 'NONE', *, *, #2387, .T. ) ;
#9357=VECTOR ( 'NONE', #3706, 1000.000000000000000 ) ;
#9384=EDGE_CURVE ( 'NONE', #8174, #18157, #7170, .T. ) ;
#9570=CARTESIAN_POINT ( 'NONE',  ( -65.62876257020761273, -24.89748912807110059, 5.000000000000000000 ) ) ;
#9571=CARTESIAN_POINT ( 'NONE',  ( -62.94070309524829554, 13.05707373847569919, -5.515665073666220062E-15 ) ) ;
#9589=EDGE_CURVE ( 'NONE', #15787, #15219, #8839, .T. ) ;
#9599=EDGE_LOOP ( 'NONE', ( #7726, #16330, #13307 ) ) ;
#9609=AXIS2_PLACEMENT_3D ( 'NONE', #9571, #16803, #22246 ) ;
#9640=VERTEX_POINT ( 'NONE', #11683 ) ;
#9641=DIRECTION ( 'NONE',  ( -0.005235963827108362431, 0.9999862922474493931, 5.936218956694023463E-19 ) ) ;
#9693=DIRECTION ( 'NONE',  ( 0.9999862922474493931, 0.005235963827108152530, 0.000000000000000000 ) ) ;
#9728=ORIENTED_EDGE ( 'NONE', *, *, #11294, .F. ) ;
#9760=ORIENTED_EDGE ( 'NONE', *, *, #3358, .T. ) ;
#9804=CONICAL_SURFACE ( 'NONE', #18515, 5.386751345948120218, 1.047197551196598297 ) ;
#9845=VERTEX_POINT ( 'NONE', #8109 ) ;
#9871=EDGE_CURVE ( 'NONE', #12983, #8958, #4885, .T. ) ;
#10015=DIRECTION ( 'NONE',  ( -0.005235963827108352890, 0.9999862922474493931, 5.936218956694023463E-19 ) ) ;
#10031=EDGE_CURVE ( 'NONE', #18157, #6518, #6096, .T. ) ;
#10034=VERTEX_POINT ( 'NONE', #13045 ) ;
#10078=DIRECTION ( 'NONE',  ( -0.8660135325225011282, -0.004534477687572232088, -0.4999999999999998890 ) ) ;
#10086=ORIENTED_EDGE ( 'NONE', *, *, #23404, .T. ) ;
#10146=VERTEX_POINT ( 'NONE', #2579 ) ;
#10148=DIRECTION ( 'NONE',  ( 5.101515458763229339E-16, 0.000000000000000000, 1.000000000000000000 ) ) ;
#10196=AXIS2_PLACEMENT_3D ( 'NONE', #19396, #2893, #22704 ) ;
#10214=VERTEX_POINT ( 'NONE', #22275 ) ;
#10215=CARTESIAN_POINT ( 'NONE',  ( -59.85533902005759899, -24.86725927682059734, -5.000000000000000000 ) ) ;
#10237=( NAMED_UNIT ( * ) PLANE_ANGLE_UNIT ( ) SI_UNIT ( $, .RADIAN. ) );
#10276=CARTESIAN_POINT ( 'NONE',  ( -62.86014019962070165, -2.329165347875060021, -5.524798807282839984E-15 ) ) ;
#10285=ORIENTED_EDGE ( 'NONE', *, *, #18353, .T. ) ;
#10288=ORIENTED_EDGE ( 'NONE', *, *, #19639, .T. ) ;
#10360=APPLICATION_CONTEXT ( 'configuration controlled 3d designs of mechanical parts and assemblies' ) ;
#10390=DIRECTION ( 'NONE',  ( 0.7107421451278728153, -0.7034526303448085383, -8.700833610568998825E-17 ) ) ;
#10411=PLANE ( 'NONE',  #14890 ) ;
#10436=DESIGN_CONTEXT ( 'detailed design', #10360, 'design' ) ;
#10452=EDGE_CURVE ( 'NONE', #16628, #8168, #20012, .T. ) ;
#10510=DIRECTION ( 'NONE',  ( -0.005235963827108352890, 0.9999862922474493931, 5.936218956694023463E-19 ) ) ;
#10512=DIRECTION ( 'NONE',  ( 0.005235963827110212514, -0.9999862922474493931, -5.936218956700083401E-19 ) ) ;
#10710=DIRECTION ( 'NONE',  ( 0.9999862922474493931, 0.005235963827108232327, -1.922962686383570719E-16 ) ) ;
#10739=FACE_OUTER_BOUND ( 'NONE', #7329, .T. ) ;
#10810=CARTESIAN_POINT ( 'NONE',  ( -65.64475015647069256, -21.84411297095480009, 5.000000000000000000 ) ) ;
#10833=EDGE_CURVE ( 'NONE', #9640, #2031, #4825, .T. ) ;
#10890=FACE_OUTER_BOUND ( 'NONE', #6864, .T. ) ;
#10902=DIRECTION ( 'NONE',  ( -7.691776389375310104E-16, -3.433811468266040107E-18, -1.000000000000000000 ) ) ;
#10973=DIRECTION ( 'NONE',  ( 0.9999862922474493931, 0.005235963827108152530, 0.000000000000000000 ) ) ;
#11042=CARTESIAN_POINT ( 'NONE',  ( -65.94066197199057910, 13.04136584699437407, -5.515665073666213751E-15 ) ) ;
#11145=EDGE_CURVE ( 'NONE', #14376, #12983, #18688, .T. ) ;
#11207=ORIENTED_EDGE ( 'NONE', *, *, #8047, .T. ) ;
#11215=CARTESIAN_POINT ( 'NONE',  ( -65.64475015647069256, -21.84411297095480009, -5.000000000000000000 ) ) ;
#11294=EDGE_CURVE ( 'NONE', #9845, #14376, #1312, .T. ) ;
#11324=DIRECTION ( 'NONE',  ( -0.005235963827108362431, 0.9999862922474493931, 5.936218956694023463E-19 ) ) ;
#11327=CARTESIAN_POINT ( 'NONE',  ( -65.33043290661754554, 13.65811943861251443, -5.515300856952130332E-15 ) ) ;
#11349=LINE ( 'NONE', #20580, #3755 ) ;
#11389=DIRECTION ( 'NONE',  ( 0.9999862922474493931, 0.005235963827108502076, 0.000000000000000000 ) ) ;
#11403=EDGE_CURVE ( 'NONE', #17399, #12644, #22609, .T. ) ;
#11405=CARTESIAN_POINT ( 'NONE',  ( -56.98461483124570037, -21.79876819407909849, -1.072991366992009803E-14 ) ) ;
#11483=DIRECTION ( 'NONE',  ( -0.005235963827108352890, 0.9999862922474493931, 5.936218956694023463E-19 ) ) ;
#11499=AXIS2_PLACEMENT_3D ( 'NONE', #7549, #10902, #7203 ) ;
#11561=ORIENTED_EDGE ( 'NONE', *, *, #18037, .T. ) ;
#11577=ORIENTED_EDGE ( 'NONE', *, *, #10031, .T. ) ;
#11614=DIRECTION ( 'NONE',  ( 0.005235963827108232327, -0.9999862922474493931, -5.936218956694023463E-19 ) ) ;
#11655=EDGE_LOOP ( 'NONE', ( #8095, #16113, #17093, #18484, #14263 ) ) ;
#11665=ORIENTED_EDGE ( 'NONE', *, *, #17872, .F. ) ;
#11683=CARTESIAN_POINT ( 'NONE',  ( -58.47878404538157326, -8.306306658711820390, -5.528360538656855117E-15 ) ) ;
#11687=ADVANCED_FACE ( 'NONE', ( #7597 ), #5617, .T. ) ;
#11888=CARTESIAN_POINT ( 'NONE',  ( -59.87132660632070014, -21.81388311970430038, 5.000000000000000000 ) ) ;
#11906=ORIENTED_EDGE ( 'NONE', *, *, #5924, .F. ) ;
#11974=EDGE_CURVE ( 'NONE', #10214, #8174, #3329, .T. ) ;
#11978=ORIENTED_EDGE ( 'NONE', *, *, #9231, .T. ) ;
#12049=FACE_OUTER_BOUND ( 'NONE', #8392, .T. ) ;
#12064=DIRECTION ( 'NONE',  ( 0.9999862922474493931, 0.005235963827110170880, 0.000000000000000000 ) ) ;
#12116=CARTESIAN_POINT ( 'NONE',  ( -62.73971250800079957, -25.32895006819559924, -5.000000000000000000 ) ) ;
#12142=DIRECTION ( 'NONE',  ( 0.005235963827108352890, -0.9999862922474493931, -5.936218956694023463E-19 ) ) ;
#12181=CARTESIAN_POINT ( 'NONE',  ( -59.85533902005759899, -24.86725927682059734, 5.000000000000000000 ) ) ;
#12198=EDGE_CURVE ( 'NONE', #12644, #15787, #1524, .T. ) ;
#12371=CARTESIAN_POINT ( 'NONE',  ( -65.64475015647069256, -21.84411297095480009, 5.000000000000000000 ) ) ;
#12413=EDGE_CURVE ( 'NONE', #17804, #8958, #3968, .T. ) ;
#12423=PLANE ( 'NONE',  #2014 ) ;
#12461=ORIENTED_EDGE ( 'NONE', *, *, #9384, .F. ) ;
#12468=EDGE_LOOP ( 'NONE', ( #3653, #14316, #7391, #23455 ) ) ;
#12512=DIRECTION ( 'NONE',  ( -0.005235963827108352890, 0.9999862922474493931, 5.936218956694023463E-19 ) ) ;
#12530=DIRECTION ( 'NONE',  ( 0.005235963827108352890, -0.9999862922474493931, -2.671135040551771006E-18 ) ) ;
#12602=ADVANCED_FACE ( 'NONE', ( #23061 ), #14340, .T. ) ;
#12614=AXIS2_PLACEMENT_3D ( 'NONE', #4558, #20163, #11389 ) ;
#12623=PLANE ( 'NONE',  #18354 ) ;
#12636=CARTESIAN_POINT ( 'NONE',  ( -65.86009907636304206, -2.344873239356385142, -5.892192847027045428E-15 ) ) ;
#12644=VERTEX_POINT ( 'NONE', #22830 ) ;
#12722=CARTESIAN_POINT ( 'NONE',  ( -62.73971250800079957, -25.32895006819559924, 5.000000000000000000 ) ) ;
#12729=ORIENTED_EDGE ( 'NONE', *, *, #20787, .F. ) ;
#12737=ADVANCED_FACE ( 'NONE', ( #9170 ), #17849, .T. ) ;
#12739=AXIS2_PLACEMENT_3D ( 'NONE', #2569, #13380, #415 ) ;
#12766=DIRECTION ( 'NONE',  ( 0.005235963827110211646, -0.9999862922474493931, -5.936218956700079549E-19 ) ) ;
#12803=FACE_OUTER_BOUND ( 'NONE', #9599, .T. ) ;
#12860=ORIENTED_EDGE ( 'NONE', *, *, #12198, .F. ) ;
#12937=ORIENTED_EDGE ( 'NONE', *, *, #16282, .T. ) ;
#12944=CARTESIAN_POINT ( 'NONE',  ( -57.73978104676354661, -25.30277024906005678, -5.538318824519921191E-15 ) ) ;
#12983=VERTEX_POINT ( 'NONE', #11215 ) ;
#13032=EDGE_CURVE ( 'NONE', #16843, #9845, #132, .T. ) ;
#13045=CARTESIAN_POINT ( 'NONE',  ( -67.06978017061331343, -25.35162245663349978, 2.500000000000000000 ) ) ;
#13192=DIRECTION ( 'NONE',  ( 0.9999862922474493931, 0.005235963827108152530, 0.000000000000000000 ) ) ;
#13273=CARTESIAN_POINT ( 'NONE',  ( -67.73964396923804543, -25.35512988733119855, 1.339745962155619363 ) ) ;
#13307=ORIENTED_EDGE ( 'NONE', *, *, #15333, .F. ) ;
#13318=VECTOR ( 'NONE', #21693, 1000.000000000000000 ) ;
#13320=( LENGTH_UNIT ( ) NAMED_UNIT ( * ) SI_UNIT ( .MILLI., .METRE. ) );
#13368=ORIENTED_EDGE ( 'NONE', *, *, #17872, .T. ) ;
#13380=DIRECTION ( 'NONE',  ( 0.000000000000000000, 0.000000000000000000, 1.000000000000000000 ) ) ;
#13388=CARTESIAN_POINT ( 'NONE',  ( -62.94230935805129690, 13.36384453327990052, -5.515482965309170069E-15 ) ) ;
#13417=VECTOR ( 'NONE', #2503, 1000.000000000000000 ) ;
#13476=CARTESIAN_POINT ( 'NONE',  ( -62.75803838139569280, -21.82899804532949872, -5.536374493610579731E-15 ) ) ;
#13520=ORIENTED_EDGE ( 'NONE', *, *, #13032, .T. ) ;
#13539=LINE ( 'NONE', #20783, #13417 ) ;
#13548=ADVANCED_FACE ( 'NONE', ( #662 ), #4082, .T. ) ;
#13557=CARTESIAN_POINT ( 'NONE',  ( -59.87132660632070014, -21.81388311970430038, -5.000000000000000000 ) ) ;
#13608=CARTESIAN_POINT ( 'NONE',  ( -62.73971250800079957, -25.32895006819559924, 5.000000000000000000 ) ) ;
#13621=LINE ( 'NONE', #22393, #19392 ) ;
#13633=PRODUCT_DEFINITION_SHAPE ( 'NONE', 'NONE',  #19552 ) ;
#13638=EDGE_LOOP ( 'NONE', ( #5408, #969 ) ) ;
#13640=ORIENTED_EDGE ( 'NONE', *, *, #11145, .T. ) ;
#13690=EDGE_CURVE ( 'NONE', #10034, #10146, #4461, .T. ) ;
#13709=FACE_OUTER_BOUND ( 'NONE', #11655, .T. ) ;
#13775=CARTESIAN_POINT ( 'NONE',  ( -62.73971250800079957, -25.32895006819559924, -5.000000000000000000 ) ) ;
#13790=CARTESIAN_POINT ( 'NONE',  ( -57.73978104676363898, -25.30277024906008521, 1.339745962155610037 ) ) ;
#13839=DIRECTION ( 'NONE',  ( -0.005235963827110212514, 0.9999862922474493931, 5.936218956700083401E-19 ) ) ;
#13841=EDGE_CURVE ( 'NONE', #22271, #16628, #6757, .T. ) ;
#13926=PLANE ( 'NONE',  #20168 ) ;
#13929=DIRECTION ( 'NONE',  ( -0.005235963827108362431, 0.9999862922474493931, 5.936218956694023463E-19 ) ) ;
#13932=ORIENTED_EDGE ( 'NONE', *, *, #8112, .F. ) ;
#13967=CARTESIAN_POINT ( 'NONE',  ( -62.73971250800079957, -25.32895006819559924, -5.538452170245418869E-15 ) ) ;
#14020=( GEOMETRIC_REPRESENTATION_CONTEXT ( 3 ) GLOBAL_UNCERTAINTY_ASSIGNED_CONTEXT ( ( #6826 ) ) GLOBAL_UNIT_ASSIGNED_CONTEXT ( ( #13320, #10237, #16992 ) ) REPRESENTATION_CONTEXT ( 'NONE', 'WORKASPACE' ) );
#14056=DIRECTION ( 'NONE',  ( 0.005235963827108352890, -0.9999862922474493931, -2.671135040551771006E-18 ) ) ;
#14061=CARTESIAN_POINT ( 'NONE',  ( -62.82872441665805496, -8.329083101359751495, -5.528360538656856695E-15 ) ) ;
#14067=CARTESIAN_POINT ( 'NONE',  ( -62.86014019962070165, -2.329165347875060021, -5.524798807282839984E-15 ) ) ;
#14108=VECTOR ( 'NONE', #8408, 1000.000000000000000 ) ;
#14121=ORIENTED_EDGE ( 'NONE', *, *, #11145, .F. ) ;
#14122=ORIENTED_EDGE ( 'NONE', *, *, #2387, .F. ) ;
#14126=ORIENTED_EDGE ( 'NONE', *, *, #20787, .T. ) ;
#14163=CARTESIAN_POINT ( 'NONE',  ( -68.53146193154570653, -21.85922789657999843, -2.680796741387739937E-15 ) ) ;
#14182=CARTESIAN_POINT ( 'NONE',  ( -59.87132660632070014, -21.81388311970430038, 5.000000000000000000 ) ) ;
#14263=ORIENTED_EDGE ( 'NONE', *, *, #8112, .T. ) ;
#14289=ORIENTED_EDGE ( 'NONE', *, *, #1567, .F. ) ;
#14296=( BOUNDED_CURVE ( )  B_SPLINE_CURVE ( 2, ( #6026, #13273, #4371 ),
 .UNSPECIFIED., .F., .F. ) 
 B_SPLINE_CURVE_WITH_KNOTS ( ( 3, 3 ),
 ( 0.000000000000000000, 0.2928548593876180162 ),
 .UNSPECIFIED. ) 
 CURVE ( )  GEOMETRIC_REPRESENTATION_ITEM ( )  RATIONAL_B_SPLINE_CURVE ( ( 1.000000000000000000, 1.037954849302039850, 1.000000000000000000 ) ) 
 REPRESENTATION_ITEM ( '' )  );
#14297=VECTOR ( 'NONE', #20684, 1000.000000000000000 ) ;
#14299=CARTESIAN_POINT ( 'NONE',  ( -58.40964484538829993, -25.30627767975780174, -2.500000000000000000 ) ) ;
#14310=CARTESIAN_POINT ( 'NONE',  ( -62.73971250800079957, -25.32895006819559924, -5.538452170245418869E-15 ) ) ;
#14316=ORIENTED_EDGE ( 'NONE', *, *, #9384, .T. ) ;
#14321=AXIS2_PLACEMENT_3D ( 'NONE', #13388, #2575, #7921 ) ;
#14340=CONICAL_SURFACE ( 'NONE', #10196, 5.386751345948120218, 1.047197551196598297 ) ;
#14376=VERTEX_POINT ( 'NONE', #8948 ) ;
#14379=ORIENTED_EDGE ( 'NONE', *, *, #2945, .F. ) ;
#14503=ORIENTED_EDGE ( 'NONE', *, *, #4181, .F. ) ;
#14505=ORIENTED_EDGE ( 'NONE', *, *, #1852, .F. ) ;
#14582=( BOUNDED_CURVE ( )  B_SPLINE_CURVE ( 2, ( #22324, #13790, #2506 ),
 .UNSPECIFIED., .F., .F. ) 
 B_SPLINE_CURVE_WITH_KNOTS ( ( 3, 3 ),
 ( 0.2928548593876180162, 0.5857097187752370315 ),
 .UNSPECIFIED. ) 
 CURVE ( )  GEOMETRIC_REPRESENTATION_ITEM ( )  RATIONAL_B_SPLINE_CURVE ( ( 1.000000000000000000, 1.037954849302049842, 1.000000000000000000 ) ) 
 REPRESENTATION_ITEM ( '' )  );
#14602=CARTESIAN_POINT ( 'NONE',  ( -68.53146193154570653, -21.85922789657999843, -2.680796741387739937E-15 ) ) ;
#14633=CARTESIAN_POINT ( 'NONE',  ( -59.87132660632070014, -21.81388311970430038, 5.000000000000000000 ) ) ;
#14639=LINE ( 'NONE', #18086, #9357 ) ;
#14650=CARTESIAN_POINT ( 'NONE',  ( -65.62876257020761273, -24.89748912807110059, -5.000000000000000000 ) ) ;
#14676=CARTESIAN_POINT ( 'NONE',  ( -62.74088165156670271, -25.10566213532069924, -5.538319619822460249E-15 ) ) ;
#14725=LINE ( 'NONE', #20662, #356 ) ;
#14757=EDGE_LOOP ( 'NONE', ( #16668, #17557, #14121, #19321, #4272 ) ) ;
#14800=CIRCLE ( 'NONE', #18563, 3.000000000000001332 ) ;
#14803=ORIENTED_EDGE ( 'NONE', *, *, #6057, .F. ) ;
#14855=EDGE_LOOP ( 'NONE', ( #4964, #13640, #3699, #11207, #22691, #13520 ) ) ;
#14890=AXIS2_PLACEMENT_3D ( 'NONE', #14182, #3362, #8367 ) ;
#14937=LINE ( 'NONE', #10810, #13318 ) ;
#14976=ORIENTED_EDGE ( 'NONE', *, *, #3528, .F. ) ;
#15063=EDGE_CURVE ( 'NONE', #18682, #9101, #17353, .T. ) ;
#15075=DIRECTION ( 'NONE',  ( 0.005235963827108352890, -0.9999862922474493931, -2.671135040551771006E-18 ) ) ;
#15143=DIRECTION ( 'NONE',  ( -0.005235963827110212514, 0.9999862922474493931, 5.936218956700083401E-19 ) ) ;
#15219=VERTEX_POINT ( 'NONE', #16494 ) ;
#15328=CIRCLE ( 'NONE', #8135, 4.349999999999996980 ) ;
#15333=EDGE_CURVE ( 'NONE', #20293, #17804, #19923, .T. ) ;
#15411=AXIS2_PLACEMENT_3D ( 'NONE', #8632, #10078, #5073 ) ;
#15599=ADVANCED_FACE ( 'NONE', ( #12803 ), #3105, .T. ) ;
#15663=ADVANCED_FACE ( 'NONE', ( #3760 ), #877, .T. ) ;
#15726=ORIENTED_EDGE ( 'NONE', *, *, #23404, .F. ) ;
#15760=CARTESIAN_POINT ( 'NONE',  ( -56.96862724498259922, -24.85214435119530307, -5.538187069399500051E-15 ) ) ;
#15770=EDGE_CURVE ( 'NONE', #15219, #12644, #8045, .T. ) ;
#15777=ORIENTED_EDGE ( 'NONE', *, *, #16282, .F. ) ;
#15787=VERTEX_POINT ( 'NONE', #12181 ) ;
#15822=CARTESIAN_POINT ( 'NONE',  ( -65.64475015647069256, -21.84411297095480009, 5.000000000000000000 ) ) ;
#15893=DIRECTION ( 'NONE',  ( 0.9999862922474493931, 0.005235963827108368503, 0.000000000000000000 ) ) ;
#16083=DIRECTION ( 'NONE',  ( 0.9999862922474492821, 0.005235963827109980928, 0.000000000000000000 ) ) ;
#16094=AXIS2_PLACEMENT_3D ( 'NONE', #23361, #8663, #15893 ) ;
#16113=ORIENTED_EDGE ( 'NONE', *, *, #1852, .T. ) ;
#16165=CARTESIAN_POINT ( 'NONE',  ( -62.75803838139569280, -21.82899804532949872, -5.120040859376149973E-15 ) ) ;
#16282=EDGE_CURVE ( 'NONE', #2031, #9640, #2754, .T. ) ;
#16330=ORIENTED_EDGE ( 'NONE', *, *, #18037, .F. ) ;
#16439=DIRECTION ( 'NONE',  ( 0.9999862922474493931, 0.005235963827108368503, 0.000000000000000000 ) ) ;
#16494=CARTESIAN_POINT ( 'NONE',  ( -58.40964484538829993, -25.30627767975780174, 2.500000000000000000 ) ) ;
#16497=CARTESIAN_POINT ( 'NONE',  ( -58.40964484538829993, -25.30627767975780174, -2.500000000000000000 ) ) ;
#16612=EDGE_LOOP ( 'NONE', ( #8256, #6395, #21910, #8988 ) ) ;
#16628=VERTEX_POINT ( 'NONE', #12944 ) ;
#16668=ORIENTED_EDGE ( 'NONE', *, *, #12413, .T. ) ;
#16715=( BOUNDED_CURVE ( )  B_SPLINE_CURVE ( 2, ( #16497, #20423, #7488 ),
 .UNSPECIFIED., .F., .F. ) 
 B_SPLINE_CURVE_WITH_KNOTS ( ( 3, 3 ),
 ( 0.2928548593876180162, 0.5857097187752360323 ),
 .UNSPECIFIED. ) 
 CURVE ( )  GEOMETRIC_REPRESENTATION_ITEM ( )  RATIONAL_B_SPLINE_CURVE ( ( 1.000000000000000000, 1.037954849302039850, 1.000000000000000000 ) ) 
 REPRESENTATION_ITEM ( '' )  );
#16732=CYLINDRICAL_SURFACE ( 'NONE', #1497, 4.349999999999996980 ) ;
#16762=CIRCLE ( 'NONE', #9609, 2.999999999999994227 ) ;
#16803=DIRECTION ( 'NONE',  ( -0.005235963827108352890, 0.9999862922474493931, 5.936218956694023463E-19 ) ) ;
#16843=VERTEX_POINT ( 'NONE', #4858 ) ;
#16850=LINE ( 'NONE', #11888, #17178 ) ;
#16855=DIRECTION ( 'NONE',  ( 0.9999862922474493931, 0.005235963827108502076, 0.000000000000000000 ) ) ;
#16858=ORIENTED_EDGE ( 'NONE', *, *, #20747, .F. ) ;
#16932=DIRECTION ( 'NONE',  ( 0.9999862922474492821, 0.005235963827109980928, 0.000000000000000000 ) ) ;
#16947=VECTOR ( 'NONE', #19127, 1000.000000000000000 ) ;
#16992=( NAMED_UNIT ( * ) SI_UNIT ( $, .STERADIAN. ) SOLID_ANGLE_UNIT ( ) );
#17055=VECTOR ( 'NONE', #18011, 999.9999999999998863 ) ;
#17093=ORIENTED_EDGE ( 'NONE', *, *, #3107, .F. ) ;
#17095=DIRECTION ( 'NONE',  ( 0.005235963827108352890, -0.9999862922474493931, -5.936218956694023463E-19 ) ) ;
#17164=CIRCLE ( 'NONE', #19073, 2.386550000000003724 ) ;
#17172=CIRCLE ( 'NONE', #2390, 4.999999999999995559 ) ;
#17178=VECTOR ( 'NONE', #2362, 1000.000000000000000 ) ;
#17253=ORIENTED_EDGE ( 'NONE', *, *, #5626, .F. ) ;
#17260=MECHANICAL_CONTEXT ( 'NONE', #5795, 'mechanical' ) ;
#17316=DIRECTION ( 'NONE',  ( 0.9999862922474493931, 0.005235963827108502076, 0.000000000000000000 ) ) ;
#17353=CIRCLE ( 'NONE', #7114, 4.349999999999996980 ) ;
#17399=VERTEX_POINT ( 'NONE', #9570 ) ;
#17473=DIRECTION ( 'NONE',  ( 0.9999862922474493931, 0.005235963827110170880, 0.000000000000000000 ) ) ;
#17548=CONICAL_SURFACE ( 'NONE', #1212, 5.386751345948120218, 1.047197551196598297 ) ;
#17557=ORIENTED_EDGE ( 'NONE', *, *, #9871, .F. ) ;
#17571=CARTESIAN_POINT ( 'NONE',  ( -61.39998491075130005, -25.32193520680032250, -5.000000000000000888 ) ) ;
#17590=CIRCLE ( 'NONE', #6584, 4.999999999999995559 ) ;
#17660=ORIENTED_EDGE ( 'NONE', *, *, #2945, .T. ) ;
#17709=EDGE_CURVE ( 'NONE', #22271, #20293, #16715, .T. ) ;
#17738=AXIS2_PLACEMENT_3D ( 'NONE', #13967, #3165, #8393 ) ;
#17804=VERTEX_POINT ( 'NONE', #13775 ) ;
#17849=CYLINDRICAL_SURFACE ( 'NONE', #22298, 4.349999999999996980 ) ;
#17872=EDGE_CURVE ( 'NONE', #10146, #17804, #521, .T. ) ;
#17920=AXIS2_PLACEMENT_3D ( 'NONE', #7608, #11324, #20667 ) ;
#17967=FACE_BOUND ( 'NONE', #13638, .T. ) ;
#18011=DIRECTION ( 'NONE',  ( 0.8633955506089472376, 0.5045276238112963441, 2.968109478347069028E-19 ) ) ;
#18015=ORIENTED_EDGE ( 'NONE', *, *, #20071, .T. ) ;
#18030=ORIENTED_EDGE ( 'NONE', *, *, #15063, .T. ) ;
#18037=EDGE_CURVE ( 'NONE', #17804, #22271, #23292, .T. ) ;
#18086=CARTESIAN_POINT ( 'NONE',  ( -58.40940726287419693, -21.55617503030518023, -5.536226058455569256E-15 ) ) ;
#18106=AXIS2_PLACEMENT_3D ( 'NONE', #5038, #10512, #12064 ) ;
#18157=VERTEX_POINT ( 'NONE', #11042 ) ;
#18179=CIRCLE ( 'NONE', #20067, 2.386550000000003724 ) ;
#18223=FACE_BOUND ( 'NONE', #4220, .T. ) ;
#18260=( BOUNDED_CURVE ( )  B_SPLINE_CURVE ( 2, ( #15760, #2932, #6857 ),
 .UNSPECIFIED., .F., .F. ) 
 B_SPLINE_CURVE_WITH_KNOTS ( ( 3, 3 ),
 ( 0.000000000000000000, 0.2928548593876180162 ),
 .UNSPECIFIED. ) 
 CURVE ( )  GEOMETRIC_REPRESENTATION_ITEM ( )  RATIONAL_B_SPLINE_CURVE ( ( 1.000000000000000000, 1.037954849302019866, 1.000000000000000000 ) ) 
 REPRESENTATION_ITEM ( '' )  );
#18353=EDGE_CURVE ( 'NONE', #5108, #10034, #14296, .T. ) ;
#18354=AXIS2_PLACEMENT_3D ( 'NONE', #16165, #23396, #9159 ) ;
#18418=DIRECTION ( 'NONE',  ( 0.9999862922474493931, 0.005235963827108152530, 0.000000000000000000 ) ) ;
#18484=ORIENTED_EDGE ( 'NONE', *, *, #13032, .F. ) ;
#18515=AXIS2_PLACEMENT_3D ( 'NONE', #14676, #20267, #3868 ) ;
#18522=AXIS2_PLACEMENT_3D ( 'NONE', #2570, #15143, #16932 ) ;
#18536=EDGE_CURVE ( 'NONE', #8168, #22271, #18260, .T. ) ;
#18547=EDGE_LOOP ( 'NONE', ( #18030, #9330, #12937, #14379 ) ) ;
#18561=ORIENTED_EDGE ( 'NONE', *, *, #3358, .F. ) ;
#18563=AXIS2_PLACEMENT_3D ( 'NONE', #14061, #13839, #16083 ) ;
#18682=VERTEX_POINT ( 'NONE', #3633 ) ;
#18688=LINE ( 'NONE', #13557, #14297 ) ;
#18706=AXIS2_PLACEMENT_3D ( 'NONE', #19155, #8335, #17473 ) ;
#18729=ADVANCED_BREP_SHAPE_REPRESENTATION ( '', ( #2022, #12739 ), #14020 ) ;
#18776=EDGE_LOOP ( 'NONE', ( #14289, #3747, #20627, #11577 ) ) ;
#18779=ORIENTED_EDGE ( 'NONE', *, *, #10452, .F. ) ;
#18817=DIRECTION ( 'NONE',  ( 0.005235963827108352890, -0.9999862922474493931, -5.936218956694023463E-19 ) ) ;
#18867=EDGE_CURVE ( 'NONE', #22209, #1782, #17164, .T. ) ;
#19000=CARTESIAN_POINT ( 'NONE',  ( -62.73971250800079957, -25.32895006819559924, -5.538452170245418869E-15 ) ) ;
#19073=AXIS2_PLACEMENT_3D ( 'NONE', #5884, #11614, #5999 ) ;
#19084=VECTOR ( 'NONE', #21833, 1000.000000000000114 ) ;
#19104=VECTOR ( 'NONE', #10710, 1000.000000000000000 ) ;
#19109=DIRECTION ( 'NONE',  ( -0.005235963827108362431, 0.9999862922474493931, 5.936218956694023463E-19 ) ) ;
#19127=DIRECTION ( 'NONE',  ( 0.005235963827108352890, -0.9999862922474493931, -5.936218956694023463E-19 ) ) ;
#19155=CARTESIAN_POINT ( 'NONE',  ( -62.82872441665799101, -8.329083101359751495, -5.528360538656857483E-15 ) ) ;
#19168=DIRECTION ( 'NONE',  ( -0.005235963827108361564, 0.9999862922474493931, 3.469446951953616307E-19 ) ) ;
#19171=( BOUNDED_CURVE ( )  B_SPLINE_CURVE ( 2, ( #19384, #3111, #8587 ),
 .UNSPECIFIED., .F., .F. ) 
 B_SPLINE_CURVE_WITH_KNOTS ( ( 3, 3 ),
 ( 0.2928548593876180162, 0.5857097187752360323 ),
 .UNSPECIFIED. ) 
 CURVE ( )  GEOMETRIC_REPRESENTATION_ITEM ( )  RATIONAL_B_SPLINE_CURVE ( ( 1.000000000000000000, 1.037954849302049842, 1.000000000000000000 ) ) 
 REPRESENTATION_ITEM ( '' )  );
#19178=CYLINDRICAL_SURFACE ( 'NONE', #614, 3.000000000000001332 ) ;
#19288=DIRECTION ( 'NONE',  ( 0.9999862922474492821, 0.005235963827108391054, 0.000000000000000000 ) ) ;
#19292=CARTESIAN_POINT ( 'NONE',  ( -62.73971250800079957, -25.32895006819559924, -5.538452170245418869E-15 ) ) ;
#19321=ORIENTED_EDGE ( 'NONE', *, *, #6057, .T. ) ;
#19325=EDGE_LOOP ( 'NONE', ( #20481, #15726, #5601 ) ) ;
#19369=AXIS2_PLACEMENT_3D ( 'NONE', #19716, #10015, #4003 ) ;
#19372=DIRECTION ( 'NONE',  ( -0.4999931461237248076, -0.002617981913554119633, -0.8660254037844385966 ) ) ;
#19384=CARTESIAN_POINT ( 'NONE',  ( -67.06978017061331343, -25.35162245663349978, 2.500000000000000000 ) ) ;
#19392=VECTOR ( 'NONE', #22279, 1000.000000000000227 ) ;
#19393=LINE ( 'NONE', #5247, #8750 ) ;
#19396=CARTESIAN_POINT ( 'NONE',  ( -62.74088165156670271, -25.10566213532069924, -5.538319619822460249E-15 ) ) ;
#19509=PLANE ( 'NONE',  #8858 ) ;
#19536=FACE_OUTER_BOUND ( 'NONE', #18776, .T. ) ;
#19552=PRODUCT_DEFINITION ( 'UNKNOWN', '', #21633, #10436 ) ;
#19554=FACE_OUTER_BOUND ( 'NONE', #8420, .T. ) ;
#19639=EDGE_CURVE ( 'NONE', #10034, #17399, #19171, .T. ) ;
#19714=AXIS2_PLACEMENT_3D ( 'NONE', #14067, #8614, #23077 ) ;
#19716=CARTESIAN_POINT ( 'NONE',  ( -62.94070309524829554, 13.05707373847569919, -5.515665073666220062E-15 ) ) ;
#19791=CARTESIAN_POINT ( 'NONE',  ( -59.86018132287835414, -2.313457456393734901, -5.524798807282839984E-15 ) ) ;
#19915=CARTESIAN_POINT ( 'NONE',  ( -59.85533902005759899, -24.86725927682059734, -5.000000000000000000 ) ) ;
#19923=( BOUNDED_CURVE ( )  B_SPLINE_CURVE ( 2, ( #10215, #17571, #12116 ),
 .UNSPECIFIED., .F., .F. ) 
 B_SPLINE_CURVE_WITH_KNOTS ( ( 3, 3 ),
 ( 0.000000000000000000, 0.2928548593876180162 ),
 .UNSPECIFIED. ) 
 CURVE ( )  GEOMETRIC_REPRESENTATION_ITEM ( )  RATIONAL_B_SPLINE_CURVE ( ( 1.000000000000000000, 1.037954849302049842, 1.000000000000000000 ) ) 
 REPRESENTATION_ITEM ( '' )  );
#19975=ADVANCED_FACE ( 'NONE', ( #20514 ), #17548, .T. ) ;
#20012=LINE ( 'NONE', #5407, #17055 ) ;
#20017=AXIS2_PLACEMENT_3D ( 'NONE', #14310, #9205, #16439 ) ;
#20067=AXIS2_PLACEMENT_3D ( 'NONE', #1927, #9068, #24 ) ;
#20071=EDGE_CURVE ( 'NONE', #10214, #6518, #3053, .T. ) ;
#20163=DIRECTION ( 'NONE',  ( -0.005235963827108362431, 0.9999862922474493931, 5.936218956694023463E-19 ) ) ;
#20168=AXIS2_PLACEMENT_3D ( 'NONE', #15822, #23052, #2037 ) ;
#20182=AXIS2_PLACEMENT_3D ( 'NONE', #9121, #3887, #7571 ) ;
#20237=CARTESIAN_POINT ( 'NONE',  ( -67.06978017061331343, -25.35162245663349978, -2.500000000000000000 ) ) ;
#20267=DIRECTION ( 'NONE',  ( -0.005235963827108362431, 0.9999862922474493931, 5.936218956694023463E-19 ) ) ;
#20293=VERTEX_POINT ( 'NONE', #19915 ) ;
#20353=CARTESIAN_POINT ( 'NONE',  ( -65.62876257020761273, -24.89748912807110059, -5.000000000000000000 ) ) ;
#20414=FACE_OUTER_BOUND ( 'NONE', #21338, .T. ) ;
#20423=CARTESIAN_POINT ( 'NONE',  ( -59.07950864401303193, -25.30978511045550050, -3.660254037844393071 ) ) ;
#20481=ORIENTED_EDGE ( 'NONE', *, *, #18353, .F. ) ;
#20514=FACE_OUTER_BOUND ( 'NONE', #21849, .T. ) ;
#20580=CARTESIAN_POINT ( 'NONE',  ( -59.87132660632070014, -21.81388311970430038, -5.000000000000000000 ) ) ;
#20627=ORIENTED_EDGE ( 'NONE', *, *, #6612, .T. ) ;
#20662=CARTESIAN_POINT ( 'NONE',  ( -68.53146193154570653, -21.85922789657999843, -2.680796741387739937E-15 ) ) ;
#20666=ORIENTED_EDGE ( 'NONE', *, *, #18867, .F. ) ;
#20667=DIRECTION ( 'NONE',  ( 0.9999862922474493931, 0.005235963827108502076, 0.000000000000000000 ) ) ;
#20684=DIRECTION ( 'NONE',  ( -0.9999862922474493931, -0.005235963827108232327, 7.691850745534263154E-16 ) ) ;
#20733=ORIENTED_EDGE ( 'NONE', *, *, #20747, .T. ) ;
#20747=EDGE_CURVE ( 'NONE', #8958, #10146, #23090, .T. ) ;
#20783=CARTESIAN_POINT ( 'NONE',  ( -65.63554743930404811, 13.34974264280344514, -5.515482965309170069E-15 ) ) ;
#20787=EDGE_CURVE ( 'NONE', #12644, #10034, #17590, .T. ) ;
#20909=CARTESIAN_POINT ( 'NONE',  ( -65.64475015647069256, -21.84411297095480009, -5.000000000000000000 ) ) ;
#20933=AXIS2_PLACEMENT_3D ( 'NONE', #1453, #14056, #1336 ) ;
#21015=ADVANCED_FACE ( 'NONE', ( #21163 ), #6929, .T. ) ;
#21119=ADVANCED_FACE ( 'NONE', ( #1326 ), #19509, .F. ) ;
#21123=ORIENTED_EDGE ( 'NONE', *, *, #13841, .T. ) ;
#21163=FACE_OUTER_BOUND ( 'NONE', #168, .T. ) ;
#21164=CARTESIAN_POINT ( 'NONE',  ( -62.74088165156670271, -25.10566213532069924, -5.538319619822460249E-15 ) ) ;
#21183=VECTOR ( 'NONE', #21864, 1000.000000000000227 ) ;
#21298=EDGE_LOOP ( 'NONE', ( #14503, #22394, #14505 ) ) ;
#21338=EDGE_LOOP ( 'NONE', ( #5258, #4665, #14803, #9728, #8309 ) ) ;
#21419=DIRECTION ( 'NONE',  ( 0.9999862922474493931, 0.005235963827108368503, 0.000000000000000000 ) ) ;
#21594=LINE ( 'NONE', #12371, #19104 ) ;
#21633=PRODUCT_DEFINITION_FORMATION_WITH_SPECIFIED_SOURCE ( 'ANY', '', #3606, .NOT_KNOWN. ) ;
#21648=CYLINDRICAL_SURFACE ( 'NONE', #19714, 3.000000000000001332 ) ;
#21693=DIRECTION ( 'NONE',  ( 0.005235963827108352890, -0.9999862922474493931, -5.936218956694023463E-19 ) ) ;
#21833=DIRECTION ( 'NONE',  ( 0.4999931461237248076, 0.002617981913554119633, 0.8660254037844385966 ) ) ;
#21849=EDGE_LOOP ( 'NONE', ( #2574, #1486, #12729 ) ) ;
#21864=DIRECTION ( 'NONE',  ( 0.4999931461237239749, 0.002617981913554110092, -0.8660254037844389297 ) ) ;
#21888=ADVANCED_FACE ( 'NONE', ( #19554 ), #1366, .T. ) ;
#21910=ORIENTED_EDGE ( 'NONE', *, *, #4023, .T. ) ;
#22016=PLANE ( 'NONE',  #11499 ) ;
#22209=VERTEX_POINT ( 'NONE', #22512 ) ;
#22246=DIRECTION ( 'NONE',  ( -0.9999862922474492821, -0.005235963827108258348, 0.000000000000000000 ) ) ;
#22262=ADVANCED_FACE ( 'NONE', ( #19536 ), #8245, .T. ) ;
#22271=VERTEX_POINT ( 'NONE', #14299 ) ;
#22275=CARTESIAN_POINT ( 'NONE',  ( -59.82876553991570034, -8.313375209878421046, -5.528360538656856695E-15 ) ) ;
#22279=DIRECTION ( 'NONE',  ( -0.4999931461237239749, -0.002617981913554110092, 0.8660254037844389297 ) ) ;
#22298=AXIS2_PLACEMENT_3D ( 'NONE', #23299, #12512, #10973 ) ;
#22324=CARTESIAN_POINT ( 'NONE',  ( -58.40964484538829993, -25.30627767975780174, 2.500000000000000000 ) ) ;
#22330=CARTESIAN_POINT ( 'NONE',  ( -58.40964484538829993, -25.30627767975780174, 2.500000000000000000 ) ) ;
#22393=CARTESIAN_POINT ( 'NONE',  ( -65.64475015647069256, -21.84411297095480009, -5.000000000000000000 ) ) ;
#22394=ORIENTED_EDGE ( 'NONE', *, *, #10452, .T. ) ;
#22414=PLANE ( 'NONE',  #7035 ) ;
#22487=CARTESIAN_POINT ( 'NONE',  ( -64.07944010525035594, -25.33596492959100033, -5.000000000000000888 ) ) ;
#22512=CARTESIAN_POINT ( 'NONE',  ( -60.55739833509119308, 13.68311121755568394, -5.807568938802639321E-15 ) ) ;
#22609=( BOUNDED_CURVE ( )  B_SPLINE_CURVE ( 2, ( #2023, #109, #12722 ),
 .UNSPECIFIED., .F., .F. ) 
 B_SPLINE_CURVE_WITH_KNOTS ( ( 3, 3 ),
 ( 0.000000000000000000, 0.2928548593876180162 ),
 .UNSPECIFIED. ) 
 CURVE ( )  GEOMETRIC_REPRESENTATION_ITEM ( )  RATIONAL_B_SPLINE_CURVE ( ( 1.000000000000000000, 1.037954849302049842, 1.000000000000000000 ) ) 
 REPRESENTATION_ITEM ( '' )  );
#22621=ORIENTED_EDGE ( 'NONE', *, *, #9589, .F. ) ;
#22649=CARTESIAN_POINT ( 'NONE',  ( -65.82868329340040248, -8.344790992841081945, -5.895754578401062139E-15 ) ) ;
#22691=ORIENTED_EDGE ( 'NONE', *, *, #7696, .T. ) ;
#22704=DIRECTION ( 'NONE',  ( 0.9999862922474493931, 0.005235963827108502076, 0.000000000000000000 ) ) ;
#22710=FACE_OUTER_BOUND ( 'NONE', #12468, .T. ) ;
#22733=CARTESIAN_POINT ( 'NONE',  ( -59.85533902005759899, -24.86725927682059734, 5.000000000000000000 ) ) ;
#22806=CARTESIAN_POINT ( 'NONE',  ( -56.98461483124570037, -21.79876819407909849, -1.072991366992009803E-14 ) ) ;
#22821=DIRECTION ( 'NONE',  ( -0.8660135325225011282, -0.004534477687572233823, 0.5000000000000000000 ) ) ;
#22830=CARTESIAN_POINT ( 'NONE',  ( -62.73971250800079957, -25.32895006819559924, 5.000000000000000000 ) ) ;
#22910=ORIENTED_EDGE ( 'NONE', *, *, #5626, .T. ) ;
#22961=SHAPE_REPRESENTATION ( 'Pin', ( #12739 ), #14020 ) ;
#23045=ADVANCED_FACE ( 'NONE', ( #20414 ), #22414, .T. ) ;
#23046=SHAPE_DEFINITION_REPRESENTATION ( #13633, #22961 ) ;
#23052=DIRECTION ( 'NONE',  ( 7.946519521424616013E-35, 4.132425482310360071E-19, 1.000000000000000000 ) ) ;
#23061=FACE_OUTER_BOUND ( 'NONE', #5692, .T. ) ;
#23077=DIRECTION ( 'NONE',  ( 0.9999862922474492821, 0.005235963827108391054, 0.000000000000000000 ) ) ;
#23090=( BOUNDED_CURVE ( )  B_SPLINE_CURVE ( 2, ( #14650, #5619, #20237 ),
 .UNSPECIFIED., .F., .F. ) 
 B_SPLINE_CURVE_WITH_KNOTS ( ( 3, 3 ),
 ( 0.000000000000000000, 0.2928548593876180162 ),
 .UNSPECIFIED. ) 
 CURVE ( )  GEOMETRIC_REPRESENTATION_ITEM ( )  RATIONAL_B_SPLINE_CURVE ( ( 1.000000000000000000, 1.037954849302039850, 1.000000000000000000 ) ) 
 REPRESENTATION_ITEM ( '' )  );
#23239=CARTESIAN_POINT ( 'NONE',  ( -67.06978017061331343, -25.35162245663349978, -2.500000000000000000 ) ) ;
#23292=CIRCLE ( 'NONE', #16094, 4.999999999999995559 ) ;
#23299=CARTESIAN_POINT ( 'NONE',  ( -62.75934763415060047, -21.57895147295310068, -5.536226058455569256E-15 ) ) ;
#23361=CARTESIAN_POINT ( 'NONE',  ( -62.73971250800079957, -25.32895006819559924, -5.538452170245418869E-15 ) ) ;
#23387=VERTEX_POINT ( 'NONE', #1496 ) ;
#23396=DIRECTION ( 'NONE',  ( -0.005235963827108231460, 0.9999862922474493931, 2.671135040551741347E-18 ) ) ;
#23404=EDGE_CURVE ( 'NONE', #10146, #5108, #8692, .T. ) ;
#23455=ORIENTED_EDGE ( 'NONE', *, *, #20071, .F. ) ;
#23536=COLOUR_RGB('Slate Gray', 0.40784314, 0.44705882, 0.49803922);
#23537=FILL_AREA_STYLE_COLOUR('',#23536);
#23538=FILL_AREA_STYLE('',(#23537));
#23539=SURFACE_STYLE_FILL_AREA(#23538);
#23540=SURFACE_SIDE_STYLE('',(#23539));
#23541=SURFACE_STYLE_USAGE(.BOTH.,#23540);
#23542=PRESENTATION_STYLE_ASSIGNMENT((#23541));
#23619=STYLED_ITEM('',(#23542),#2022);
#23620=MECHANICAL_DESIGN_GEOMETRIC_PRESENTATION_REPRESENTATION('',(#23619),#14020);
ENDSEC;
END-ISO-10303-21;
